ISO-10303-21;
HEADER;
/* Generated by software containing ST-Developer
 * from STEP Tools, Inc. (www.steptools.com) 
 */

FILE_DESCRIPTION(
/* description */ ('Low-profile wedge edge clamp'),
/* implementation_level */ '2;1');

FILE_NAME(
/* name */ 'Flat Washer - M8.step',
/* time_stamp */ '2026-10-29T15:58:13-07:00',
/* author */ (''),
/* organization */ (''),
/* preprocessor_version */ 'ST-DEVELOPER v20.2',
/* originating_system */ 'Autodesk Translation Framework v15.17.0.0',
/* authorisation */ '');

FILE_SCHEMA (('AUTOMOTIVE_DESIGN { 1 0 10303 214 3 1 1 }'));
ENDSEC;

DATA;
#10=MECHANICAL_DESIGN_GEOMETRIC_PRESENTATION_REPRESENTATION('',(#83),#2996);
#71=SHAPE_REPRESENTATION_RELATIONSHIP('SRR','None',#3033,#77);
#77=ADVANCED_BREP_SHAPE_REPRESENTATION('',(#88),#2994);
#83=STYLED_ITEM('',(#3133),#88);
#88=MANIFOLD_SOLID_BREP('Body1',#1713);
#159=FACE_BOUND('',#450,.T.);
#160=FACE_BOUND('',#452,.T.);
#197=PLANE('',#1953);
#198=PLANE('',#1954);
#285=FACE_OUTER_BOUND('',#447,.T.);
#286=FACE_OUTER_BOUND('',#448,.T.);
#287=FACE_OUTER_BOUND('',#449,.T.);
#288=FACE_OUTER_BOUND('',#451,.T.);
#447=EDGE_LOOP('',(#1511,#1512,#1513,#1514));
#448=EDGE_LOOP('',(#1515,#1516,#1517,#1518));
#449=EDGE_LOOP('',(#1519));
#450=EDGE_LOOP('',(#1520));
#451=EDGE_LOOP('',(#1521));
#452=EDGE_LOOP('',(#1522));
#568=LINE('',#2893,#687);
#569=LINE('',#2899,#688);
#687=VECTOR('',#2418,0.42);
#688=VECTOR('',#2425,0.8);
#782=CIRCLE('',#1948,0.42);
#783=CIRCLE('',#1949,0.42);
#784=CIRCLE('',#1951,0.8);
#785=CIRCLE('',#1952,0.8);
#911=VERTEX_POINT('',#2890);
#912=VERTEX_POINT('',#2892);
#913=VERTEX_POINT('',#2896);
#914=VERTEX_POINT('',#2898);
#1114=EDGE_CURVE('',#911,#911,#782,.T.);
#1115=EDGE_CURVE('',#911,#912,#568,.T.);
#1116=EDGE_CURVE('',#912,#912,#783,.T.);
#1117=EDGE_CURVE('',#913,#913,#784,.T.);
#1118=EDGE_CURVE('',#913,#914,#569,.T.);
#1119=EDGE_CURVE('',#914,#914,#785,.T.);
#1511=ORIENTED_EDGE('',*,*,#1114,.F.);
#1512=ORIENTED_EDGE('',*,*,#1115,.T.);
#1513=ORIENTED_EDGE('',*,*,#1116,.T.);
#1514=ORIENTED_EDGE('',*,*,#1115,.F.);
#1515=ORIENTED_EDGE('',*,*,#1117,.F.);
#1516=ORIENTED_EDGE('',*,*,#1118,.T.);
#1517=ORIENTED_EDGE('',*,*,#1119,.T.);
#1518=ORIENTED_EDGE('',*,*,#1118,.F.);
#1519=ORIENTED_EDGE('',*,*,#1117,.T.);
#1520=ORIENTED_EDGE('',*,*,#1114,.T.);
#1521=ORIENTED_EDGE('',*,*,#1119,.F.);
#1522=ORIENTED_EDGE('',*,*,#1116,.F.);
#1612=CYLINDRICAL_SURFACE('',#1947,0.42);
#1613=CYLINDRICAL_SURFACE('',#1950,0.8);
#1692=ADVANCED_FACE('',(#285),#1612,.F.);
#1693=ADVANCED_FACE('',(#286),#1613,.T.);
#1694=ADVANCED_FACE('',(#287,#159),#197,.T.);
#1695=ADVANCED_FACE('',(#288,#160),#198,.F.);
#1713=CLOSED_SHELL('',(#1692,#1693,#1694,#1695));
#1946=AXIS2_PLACEMENT_3D('',#2888,#2412,#2413);
#1947=AXIS2_PLACEMENT_3D('',#2889,#2414,#2415);
#1948=AXIS2_PLACEMENT_3D('',#2891,#2416,#2417);
#1949=AXIS2_PLACEMENT_3D('',#2894,#2419,#2420);
#1950=AXIS2_PLACEMENT_3D('',#2895,#2421,#2422);
#1951=AXIS2_PLACEMENT_3D('',#2897,#2423,#2424);
#1952=AXIS2_PLACEMENT_3D('',#2900,#2426,#2427);
#1953=AXIS2_PLACEMENT_3D('',#2901,#2428,#2429);
#1954=AXIS2_PLACEMENT_3D('',#2902,#2430,#2431);
#2412=DIRECTION('axis',(0.,0.,1.));
#2413=DIRECTION('refdir',(1.,0.,0.));
#2414=DIRECTION('center_axis',(0.,1.,0.));
#2415=DIRECTION('ref_axis',(1.,0.,0.));
#2416=DIRECTION('center_axis',(0.,-1.,0.));
#2417=DIRECTION('ref_axis',(1.,0.,0.));
#2418=DIRECTION('',(0.,-1.,0.));
#2419=DIRECTION('center_axis',(0.,-1.,0.));
#2420=DIRECTION('ref_axis',(1.,0.,0.));
#2421=DIRECTION('center_axis',(0.,1.,0.));
#2422=DIRECTION('ref_axis',(1.,0.,0.));
#2423=DIRECTION('center_axis',(0.,1.,0.));
#2424=DIRECTION('ref_axis',(1.,0.,0.));
#2425=DIRECTION('',(0.,-1.,0.));
#2426=DIRECTION('center_axis',(0.,1.,0.));
#2427=DIRECTION('ref_axis',(1.,0.,0.));
#2428=DIRECTION('center_axis',(0.,1.,0.));
#2429=DIRECTION('ref_axis',(1.,0.,0.));
#2430=DIRECTION('center_axis',(0.,1.,0.));
#2431=DIRECTION('ref_axis',(1.,0.,0.));
#2888=CARTESIAN_POINT('',(0.,0.,0.));
#2889=CARTESIAN_POINT('Origin',(0.,0.,0.));
#2890=CARTESIAN_POINT('',(-0.42,0.16,5.14351655641888E-17));
#2891=CARTESIAN_POINT('Origin',(0.,0.16,0.));
#2892=CARTESIAN_POINT('',(-0.42,0.,5.14351655641888E-17));
#2893=CARTESIAN_POINT('',(-0.42,0.,5.14351655641888E-17));
#2894=CARTESIAN_POINT('Origin',(0.,0.,0.));
#2895=CARTESIAN_POINT('Origin',(0.,0.,0.));
#2896=CARTESIAN_POINT('',(-0.8,0.16,9.79717439317883E-17));
#2897=CARTESIAN_POINT('Origin',(0.,0.16,0.));
#2898=CARTESIAN_POINT('',(-0.8,0.,9.79717439317883E-17));
#2899=CARTESIAN_POINT('',(-0.8,0.,9.79717439317883E-17));
#2900=CARTESIAN_POINT('Origin',(0.,0.,0.));
#2901=CARTESIAN_POINT('Origin',(0.,0.16,0.));
#2902=CARTESIAN_POINT('Origin',(0.,0.,0.));
#2985=UNCERTAINTY_MEASURE_WITH_UNIT(LENGTH_MEASURE(0.001),#2997,
'DISTANCE_ACCURACY_VALUE',
'Maximum model space distance between geometric entities at asserted c
onnectivities');
#2987=UNCERTAINTY_MEASURE_WITH_UNIT(LENGTH_MEASURE(0.001),#2997,
'DISTANCE_ACCURACY_VALUE',
'Maximum model space distance between geometric entities at asserted c
onnectivities');
#2994=(
GEOMETRIC_REPRESENTATION_CONTEXT(3)
GLOBAL_UNCERTAINTY_ASSIGNED_CONTEXT((#2985))
GLOBAL_UNIT_ASSIGNED_CONTEXT((#2997,#2999,#3000))
REPRESENTATION_CONTEXT('','3D')
);
#2996=(
GEOMETRIC_REPRESENTATION_CONTEXT(3)
GLOBAL_UNCERTAINTY_ASSIGNED_CONTEXT((#2987))
GLOBAL_UNIT_ASSIGNED_CONTEXT((#2997,#2999,#3000))
REPRESENTATION_CONTEXT('','3D')
);
#2997=(
LENGTH_UNIT()
NAMED_UNIT(*)
SI_UNIT(.CENTI.,.METRE.)
);
#2999=(
NAMED_UNIT(*)
PLANE_ANGLE_UNIT()
SI_UNIT($,.RADIAN.)
);
#3000=(
NAMED_UNIT(*)
SI_UNIT($,.STERADIAN.)
SOLID_ANGLE_UNIT()
);
#3007=SHAPE_DEFINITION_REPRESENTATION(#3015,#3033);
#3015=PRODUCT_DEFINITION_SHAPE('',$,#3042);
#3033=SHAPE_REPRESENTATION('',(#1946),#2994);
#3035=PRODUCT_DEFINITION_CONTEXT('part definition',#3061,'design');
#3042=PRODUCT_DEFINITION('Flat Washer - M8','Flat Washer - M8',#3050,#3035);
#3050=PRODUCT_DEFINITION_FORMATION('',$,#3069);
#3061=APPLICATION_CONTEXT(
'Core Data for Automotive Mechanical Design Process');
#3062=PRODUCT_CONTEXT('part definition',#3061,'mechanical');
#3069=PRODUCT('Flat Washer - M8','Flat Washer - M8','Flat Washer - M8',
(#3062));
#3127=COLOUR_RGB('Black',0.12,0.14,0.17);
#3128=FILL_AREA_STYLE_COLOUR('',#3127);
#3129=FILL_AREA_STYLE('',(#3128));
#3130=SURFACE_STYLE_FILL_AREA(#3129);
#3131=SURFACE_SIDE_STYLE('',(#3130));
#3132=SURFACE_STYLE_USAGE(.BOTH.,#3131);
#3133=PRESENTATION_STYLE_ASSIGNMENT((#3132));
ENDSEC;
END-ISO-10303-21;
